ISO-10303-21;
HEADER;
/* Generated by software containing ST-Developer
 * from STEP Tools, Inc. (www.steptools.com) 
 */

FILE_DESCRIPTION(
/* description */ ('Located fixture plate with toggle clamp'),
/* implementation_level */ '2;1');

FILE_NAME(
/* name */ 'Flat Washer - M5.step',
/* time_stamp */ '2026-10-27T21:36:12-07:00',
/* author */ (''),
/* organization */ (''),
/* preprocessor_version */ 'ST-DEVELOPER v20.2',
/* originating_system */ 'Autodesk Translation Framework v15.17.0.0',
/* authorisation */ '');

FILE_SCHEMA (('AUTOMOTIVE_DESIGN { 1 0 10303 214 3 1 1 }'));
ENDSEC;

DATA;
#10=MECHANICAL_DESIGN_GEOMETRIC_PRESENTATION_REPRESENTATION('',(#323),#9285);
#250=CONICAL_SURFACE('',#5547,0.275,0.785398163397449);
#275=SHAPE_REPRESENTATION_RELATIONSHIP('SRR','None',#9398,#299);
#299=ADVANCED_BREP_SHAPE_REPRESENTATION('',(#347),#9260);
#323=STYLED_ITEM('',(#9619),#347);
#347=MANIFOLD_SOLID_BREP('Body1',#5171);
#385=FACE_BOUND('',#1047,.T.);
#386=FACE_BOUND('',#1050,.T.);
#532=PLANE('',#5552);
#533=PLANE('',#5556);
#730=FACE_OUTER_BOUND('',#1044,.T.);
#731=FACE_OUTER_BOUND('',#1045,.T.);
#732=FACE_OUTER_BOUND('',#1046,.T.);
#733=FACE_OUTER_BOUND('',#1048,.T.);
#734=FACE_OUTER_BOUND('',#1049,.T.);
#1044=EDGE_LOOP('',(#3772,#3773,#3774,#3775));
#1045=EDGE_LOOP('',(#3776,#3777,#3778,#3779));
#1046=EDGE_LOOP('',(#3780));
#1047=EDGE_LOOP('',(#3781));
#1048=EDGE_LOOP('',(#3782,#3783,#3784,#3785));
#1049=EDGE_LOOP('',(#3786));
#1050=EDGE_LOOP('',(#3787));
#1407=CIRCLE('',#5548,0.285);
#1408=CIRCLE('',#5549,0.265);
#1409=CIRCLE('',#5551,0.265);
#1410=CIRCLE('',#5553,0.5);
#1411=CIRCLE('',#5555,0.5);
#1701=LINE('',#7881,#2111);
#1702=LINE('',#7885,#2112);
#1703=LINE('',#7892,#2113);
#2111=VECTOR('',#6325,0.275);
#2112=VECTOR('',#6330,0.265);
#2113=VECTOR('',#6339,0.5);
#2497=VERTEX_POINT('',#7878);
#2498=VERTEX_POINT('',#7880);
#2499=VERTEX_POINT('',#7884);
#2500=VERTEX_POINT('',#7888);
#2501=VERTEX_POINT('',#7891);
#2974=EDGE_CURVE('',#2497,#2497,#1407,.T.);
#2975=EDGE_CURVE('',#2497,#2498,#1701,.T.);
#2976=EDGE_CURVE('',#2498,#2498,#1408,.T.);
#2977=EDGE_CURVE('',#2498,#2499,#1702,.T.);
#2978=EDGE_CURVE('',#2499,#2499,#1409,.T.);
#2979=EDGE_CURVE('',#2500,#2500,#1410,.T.);
#2980=EDGE_CURVE('',#2500,#2501,#1703,.T.);
#2981=EDGE_CURVE('',#2501,#2501,#1411,.T.);
#3772=ORIENTED_EDGE('',*,*,#2974,.T.);
#3773=ORIENTED_EDGE('',*,*,#2975,.T.);
#3774=ORIENTED_EDGE('',*,*,#2976,.T.);
#3775=ORIENTED_EDGE('',*,*,#2975,.F.);
#3776=ORIENTED_EDGE('',*,*,#2976,.F.);
#3777=ORIENTED_EDGE('',*,*,#2977,.T.);
#3778=ORIENTED_EDGE('',*,*,#2978,.T.);
#3779=ORIENTED_EDGE('',*,*,#2977,.F.);
#3780=ORIENTED_EDGE('',*,*,#2979,.T.);
#3781=ORIENTED_EDGE('',*,*,#2974,.F.);
#3782=ORIENTED_EDGE('',*,*,#2979,.F.);
#3783=ORIENTED_EDGE('',*,*,#2980,.T.);
#3784=ORIENTED_EDGE('',*,*,#2981,.T.);
#3785=ORIENTED_EDGE('',*,*,#2980,.F.);
#3786=ORIENTED_EDGE('',*,*,#2981,.F.);
#3787=ORIENTED_EDGE('',*,*,#2978,.F.);
#4803=CYLINDRICAL_SURFACE('',#5550,0.265);
#4804=CYLINDRICAL_SURFACE('',#5554,0.5);
#4931=ADVANCED_FACE('',(#730),#250,.F.);
#4932=ADVANCED_FACE('',(#731),#4803,.F.);
#4933=ADVANCED_FACE('',(#732,#385),#532,.T.);
#4934=ADVANCED_FACE('',(#733),#4804,.T.);
#4935=ADVANCED_FACE('',(#734,#386),#533,.F.);
#5171=CLOSED_SHELL('',(#4931,#4932,#4933,#4934,#4935));
#5546=AXIS2_PLACEMENT_3D('',#7876,#6319,#6320);
#5547=AXIS2_PLACEMENT_3D('',#7877,#6321,#6322);
#5548=AXIS2_PLACEMENT_3D('',#7879,#6323,#6324);
#5549=AXIS2_PLACEMENT_3D('',#7882,#6326,#6327);
#5550=AXIS2_PLACEMENT_3D('',#7883,#6328,#6329);
#5551=AXIS2_PLACEMENT_3D('',#7886,#6331,#6332);
#5552=AXIS2_PLACEMENT_3D('',#7887,#6333,#6334);
#5553=AXIS2_PLACEMENT_3D('',#7889,#6335,#6336);
#5554=AXIS2_PLACEMENT_3D('',#7890,#6337,#6338);
#5555=AXIS2_PLACEMENT_3D('',#7893,#6340,#6341);
#5556=AXIS2_PLACEMENT_3D('',#7894,#6342,#6343);
#6319=DIRECTION('axis',(0.,0.,1.));
#6320=DIRECTION('refdir',(1.,0.,0.));
#6321=DIRECTION('center_axis',(0.,1.,0.));
#6322=DIRECTION('ref_axis',(1.,0.,0.));
#6323=DIRECTION('center_axis',(0.,1.,0.));
#6324=DIRECTION('ref_axis',(1.,0.,0.));
#6325=DIRECTION('',(0.707106781186548,-0.707106781186547,-8.65956056235494E-17));
#6326=DIRECTION('center_axis',(0.,-1.,0.));
#6327=DIRECTION('ref_axis',(1.,0.,0.));
#6328=DIRECTION('center_axis',(0.,1.,0.));
#6329=DIRECTION('ref_axis',(1.,0.,0.));
#6330=DIRECTION('',(0.,-1.,0.));
#6331=DIRECTION('center_axis',(0.,-1.,0.));
#6332=DIRECTION('ref_axis',(1.,0.,0.));
#6333=DIRECTION('center_axis',(0.,1.,0.));
#6334=DIRECTION('ref_axis',(1.,0.,0.));
#6335=DIRECTION('center_axis',(0.,1.,0.));
#6336=DIRECTION('ref_axis',(1.,0.,0.));
#6337=DIRECTION('center_axis',(0.,1.,0.));
#6338=DIRECTION('ref_axis',(1.,0.,0.));
#6339=DIRECTION('',(0.,-1.,0.));
#6340=DIRECTION('center_axis',(0.,1.,0.));
#6341=DIRECTION('ref_axis',(1.,0.,0.));
#6342=DIRECTION('center_axis',(0.,1.,0.));
#6343=DIRECTION('ref_axis',(1.,0.,0.));
#7876=CARTESIAN_POINT('',(0.,0.,0.));
#7877=CARTESIAN_POINT('Origin',(0.,0.09,0.));
#7878=CARTESIAN_POINT('',(-0.285,0.1,3.49024337756996E-17));
#7879=CARTESIAN_POINT('Origin',(0.,0.1,0.));
#7880=CARTESIAN_POINT('',(-0.265,0.08,-3.24531401774049E-17));
#7881=CARTESIAN_POINT('',(-0.275,0.09,3.36777869765522E-17));
#7882=CARTESIAN_POINT('Origin',(0.,0.08,0.));
#7883=CARTESIAN_POINT('Origin',(0.,0.,0.));
#7884=CARTESIAN_POINT('',(-0.265,0.,3.24531401774049E-17));
#7885=CARTESIAN_POINT('',(-0.265,0.,3.24531401774049E-17));
#7886=CARTESIAN_POINT('Origin',(0.,0.,0.));
#7887=CARTESIAN_POINT('Origin',(0.,0.1,0.));
#7888=CARTESIAN_POINT('',(-0.5,0.1,6.12323399573677E-17));
#7889=CARTESIAN_POINT('Origin',(0.,0.1,0.));
#7890=CARTESIAN_POINT('Origin',(0.,0.,0.));
#7891=CARTESIAN_POINT('',(-0.5,0.,6.12323399573677E-17));
#7892=CARTESIAN_POINT('',(-0.5,0.,6.12323399573677E-17));
#7893=CARTESIAN_POINT('Origin',(0.,0.,0.));
#7894=CARTESIAN_POINT('Origin',(0.,0.,0.));
#9230=UNCERTAINTY_MEASURE_WITH_UNIT(LENGTH_MEASURE(0.001),#9286,
'DISTANCE_ACCURACY_VALUE',
'Maximum model space distance between geometric entities at asserted c
onnectivities');
#9255=UNCERTAINTY_MEASURE_WITH_UNIT(LENGTH_MEASURE(0.001),#9286,
'DISTANCE_ACCURACY_VALUE',
'Maximum model space distance between geometric entities at asserted c
onnectivities');
#9260=(
GEOMETRIC_REPRESENTATION_CONTEXT(3)
GLOBAL_UNCERTAINTY_ASSIGNED_CONTEXT((#9230))
GLOBAL_UNIT_ASSIGNED_CONTEXT((#9286,#9288,#9289))
REPRESENTATION_CONTEXT('','3D')
);
#9285=(
GEOMETRIC_REPRESENTATION_CONTEXT(3)
GLOBAL_UNCERTAINTY_ASSIGNED_CONTEXT((#9255))
GLOBAL_UNIT_ASSIGNED_CONTEXT((#9286,#9288,#9289))
REPRESENTATION_CONTEXT('','3D')
);
#9286=(
LENGTH_UNIT()
NAMED_UNIT(*)
SI_UNIT(.CENTI.,.METRE.)
);
#9288=(
NAMED_UNIT(*)
PLANE_ANGLE_UNIT()
SI_UNIT($,.RADIAN.)
);
#9289=(
NAMED_UNIT(*)
SI_UNIT($,.STERADIAN.)
SOLID_ANGLE_UNIT()
);
#9294=SHAPE_DEFINITION_REPRESENTATION(#9323,#9398);
#9323=PRODUCT_DEFINITION_SHAPE('',$,#9428);
#9398=SHAPE_REPRESENTATION('',(#5546),#9260);
#9423=PRODUCT_DEFINITION_CONTEXT('part definition',#9512,'design');
#9428=PRODUCT_DEFINITION('Flat Washer - M5','Flat Washer - M5',#9457,#9423);
#9457=PRODUCT_DEFINITION_FORMATION('',$,#9518);
#9512=APPLICATION_CONTEXT(
'Core Data for Automotive Mechanical Design Process');
#9513=PRODUCT_CONTEXT('part definition',#9512,'mechanical');
#9518=PRODUCT('Flat Washer - M5','Flat Washer - M5','Flat Washer - M5',
(#9513));
#9613=COLOUR_RGB('Black',0.12,0.14,0.17);
#9614=FILL_AREA_STYLE_COLOUR('',#9613);
#9615=FILL_AREA_STYLE('',(#9614));
#9616=SURFACE_STYLE_FILL_AREA(#9615);
#9617=SURFACE_SIDE_STYLE('',(#9616));
#9618=SURFACE_STYLE_USAGE(.BOTH.,#9617);
#9619=PRESENTATION_STYLE_ASSIGNMENT((#9618));
ENDSEC;
END-ISO-10303-21;
